ISO-10303-21;
HEADER;
/* Generated by software containing ST-Developer
 * from STEP Tools, Inc. (www.steptools.com) 
 */

FILE_DESCRIPTION(
/* description */ ('Timing belt drive module 2 mm Pitch Timing 20T-40T'),

/* implementation_level */ '2;1');

FILE_NAME(
/* name */ 'M4 clamp nut (3).step',
/* time_stamp */ '2026-10-28T03:25:12-07:00',
/* author */ (''),
/* organization */ (''),
/* preprocessor_version */ 'ST-DEVELOPER v20.2',
/* originating_system */ 'Autodesk Translation Framework v15.17.0.0',
/* authorisation */ '');

FILE_SCHEMA (('AUTOMOTIVE_DESIGN { 1 0 10303 214 3 1 1 }'));
ENDSEC;

DATA;
#10=MECHANICAL_DESIGN_GEOMETRIC_PRESENTATION_REPRESENTATION('',(#535),#17830);
#449=SHAPE_REPRESENTATION_RELATIONSHIP('SRR','None',#18019,#492);
#492=ADVANCED_BREP_SHAPE_REPRESENTATION('',(#593),#17794);
#535=STYLED_ITEM('',(#18324),#593);
#593=MANIFOLD_SOLID_BREP('Body1',#8992);
#697=FACE_BOUND('',#1668,.T.);
#698=FACE_BOUND('',#1670,.T.);
#837=PLANE('',#9778);
#838=PLANE('',#9779);
#1084=FACE_OUTER_BOUND('',#1665,.T.);
#1085=FACE_OUTER_BOUND('',#1666,.T.);
#1086=FACE_OUTER_BOUND('',#1667,.T.);
#1087=FACE_OUTER_BOUND('',#1669,.T.);
#1665=EDGE_LOOP('',(#6349,#6350,#6351,#6352));
#1666=EDGE_LOOP('',(#6353,#6354,#6355,#6356));
#1667=EDGE_LOOP('',(#6357));
#1668=EDGE_LOOP('',(#6358));
#1669=EDGE_LOOP('',(#6359));
#1670=EDGE_LOOP('',(#6360));
#2260=CIRCLE('',#9773,0.164999999999999);
#2261=CIRCLE('',#9774,0.164999999999999);
#2262=CIRCLE('',#9776,0.4);
#2263=CIRCLE('',#9777,0.4);
#2958=LINE('',#14493,#3436);
#2959=LINE('',#14499,#3437);
#3436=VECTOR('',#11493,0.164999999999999);
#3437=VECTOR('',#11500,0.4);
#3938=VERTEX_POINT('',#14490);
#3939=VERTEX_POINT('',#14492);
#3940=VERTEX_POINT('',#14496);
#3941=VERTEX_POINT('',#14498);
#4857=EDGE_CURVE('',#3938,#3938,#2260,.T.);
#4858=EDGE_CURVE('',#3938,#3939,#2958,.T.);
#4859=EDGE_CURVE('',#3939,#3939,#2261,.T.);
#4860=EDGE_CURVE('',#3940,#3940,#2262,.T.);
#4861=EDGE_CURVE('',#3940,#3941,#2959,.T.);
#4862=EDGE_CURVE('',#3941,#3941,#2263,.T.);
#6349=ORIENTED_EDGE('',*,*,#4857,.F.);
#6350=ORIENTED_EDGE('',*,*,#4858,.T.);
#6351=ORIENTED_EDGE('',*,*,#4859,.T.);
#6352=ORIENTED_EDGE('',*,*,#4858,.F.);
#6353=ORIENTED_EDGE('',*,*,#4860,.F.);
#6354=ORIENTED_EDGE('',*,*,#4861,.T.);
#6355=ORIENTED_EDGE('',*,*,#4862,.T.);
#6356=ORIENTED_EDGE('',*,*,#4861,.F.);
#6357=ORIENTED_EDGE('',*,*,#4860,.T.);
#6358=ORIENTED_EDGE('',*,*,#4857,.T.);
#6359=ORIENTED_EDGE('',*,*,#4862,.F.);
#6360=ORIENTED_EDGE('',*,*,#4859,.F.);
#8239=CYLINDRICAL_SURFACE('',#9772,0.164999999999999);
#8240=CYLINDRICAL_SURFACE('',#9775,0.4);
#8582=ADVANCED_FACE('',(#1084),#8239,.F.);
#8583=ADVANCED_FACE('',(#1085),#8240,.T.);
#8584=ADVANCED_FACE('',(#1086,#697),#837,.T.);
#8585=ADVANCED_FACE('',(#1087,#698),#838,.F.);
#8992=CLOSED_SHELL('',(#8582,#8583,#8584,#8585));
#9771=AXIS2_PLACEMENT_3D('',#14488,#11487,#11488);
#9772=AXIS2_PLACEMENT_3D('',#14489,#11489,#11490);
#9773=AXIS2_PLACEMENT_3D('',#14491,#11491,#11492);
#9774=AXIS2_PLACEMENT_3D('',#14494,#11494,#11495);
#9775=AXIS2_PLACEMENT_3D('',#14495,#11496,#11497);
#9776=AXIS2_PLACEMENT_3D('',#14497,#11498,#11499);
#9777=AXIS2_PLACEMENT_3D('',#14500,#11501,#11502);
#9778=AXIS2_PLACEMENT_3D('',#14501,#11503,#11504);
#9779=AXIS2_PLACEMENT_3D('',#14502,#11505,#11506);
#11487=DIRECTION('axis',(0.,0.,1.));
#11488=DIRECTION('refdir',(1.,0.,0.));
#11489=DIRECTION('center_axis',(0.,0.,1.));
#11490=DIRECTION('ref_axis',(1.,0.,0.));
#11491=DIRECTION('center_axis',(0.,0.,-1.));
#11492=DIRECTION('ref_axis',(1.,0.,0.));
#11493=DIRECTION('',(0.,0.,-1.));
#11494=DIRECTION('center_axis',(0.,0.,-1.));
#11495=DIRECTION('ref_axis',(1.,0.,0.));
#11496=DIRECTION('center_axis',(0.,0.,1.));
#11497=DIRECTION('ref_axis',(1.,0.,0.));
#11498=DIRECTION('center_axis',(0.,0.,1.));
#11499=DIRECTION('ref_axis',(1.,0.,0.));
#11500=DIRECTION('',(0.,0.,-1.));
#11501=DIRECTION('center_axis',(0.,0.,1.));
#11502=DIRECTION('ref_axis',(1.,0.,0.));
#11503=DIRECTION('center_axis',(0.,0.,1.));
#11504=DIRECTION('ref_axis',(1.,0.,0.));
#11505=DIRECTION('center_axis',(0.,0.,1.));
#11506=DIRECTION('ref_axis',(1.,0.,0.));
#14488=CARTESIAN_POINT('',(0.,0.,0.));
#14489=CARTESIAN_POINT('Origin',(9.77091003018116,1.,-1.6));
#14490=CARTESIAN_POINT('',(9.60591003018116,1.,-1.2));
#14491=CARTESIAN_POINT('Origin',(9.77091003018116,1.,-1.2));
#14492=CARTESIAN_POINT('',(9.60591003018116,1.,-1.6));
#14493=CARTESIAN_POINT('',(9.60591003018116,1.,-1.6));
#14494=CARTESIAN_POINT('Origin',(9.77091003018116,1.,-1.6));
#14495=CARTESIAN_POINT('Origin',(9.77091003018116,1.,-1.6));
#14496=CARTESIAN_POINT('',(9.37091003018116,1.,-1.2));
#14497=CARTESIAN_POINT('Origin',(9.77091003018116,1.,-1.2));
#14498=CARTESIAN_POINT('',(9.37091003018116,1.,-1.6));
#14499=CARTESIAN_POINT('',(9.37091003018116,1.,-1.6));
#14500=CARTESIAN_POINT('Origin',(9.77091003018116,1.,-1.6));
#14501=CARTESIAN_POINT('Origin',(9.77091003018116,1.,-1.2));
#14502=CARTESIAN_POINT('Origin',(9.77091003018116,1.,-1.6));
#17744=UNCERTAINTY_MEASURE_WITH_UNIT(LENGTH_MEASURE(0.001),#17831,
'DISTANCE_ACCURACY_VALUE',
'Maximum model space distance between geometric entities at asserted c
onnectivities');
#17780=UNCERTAINTY_MEASURE_WITH_UNIT(LENGTH_MEASURE(0.001),#17831,
'DISTANCE_ACCURACY_VALUE',
'Maximum model space distance between geometric entities at asserted c
onnectivities');
#17794=(
GEOMETRIC_REPRESENTATION_CONTEXT(3)
GLOBAL_UNCERTAINTY_ASSIGNED_CONTEXT((#17744))
GLOBAL_UNIT_ASSIGNED_CONTEXT((#17831,#17833,#17834))
REPRESENTATION_CONTEXT('','3D')
);
#17830=(
GEOMETRIC_REPRESENTATION_CONTEXT(3)
GLOBAL_UNCERTAINTY_ASSIGNED_CONTEXT((#17780))
GLOBAL_UNIT_ASSIGNED_CONTEXT((#17831,#17833,#17834))
REPRESENTATION_CONTEXT('','3D')
);
#17831=(
LENGTH_UNIT()
NAMED_UNIT(*)
SI_UNIT(.CENTI.,.METRE.)
);
#17833=(
NAMED_UNIT(*)
PLANE_ANGLE_UNIT()
SI_UNIT($,.RADIAN.)
);
#17834=(
NAMED_UNIT(*)
SI_UNIT($,.STERADIAN.)
SOLID_ANGLE_UNIT()
);
#17848=SHAPE_DEFINITION_REPRESENTATION(#17897,#18019);
#17897=PRODUCT_DEFINITION_SHAPE('',$,#18069);
#18019=SHAPE_REPRESENTATION('',(#9771),#17794);
#18055=PRODUCT_DEFINITION_CONTEXT('part definition',#18204,'design');
#18069=PRODUCT_DEFINITION('M4 clamp nut (3)','M4 clamp nut (3)',#18118,#18055);
#18118=PRODUCT_DEFINITION_FORMATION('',$,#18219);
#18204=APPLICATION_CONTEXT(
'Core Data for Automotive Mechanical Design Process');
#18205=PRODUCT_CONTEXT('part definition',#18204,'mechanical');
#18219=PRODUCT('M4 clamp nut (3)','M4 clamp nut (3)','M4 clamp nut (3)',(#18205));
#18318=COLOUR_RGB('Black',0.12,0.14,0.17);
#18319=FILL_AREA_STYLE_COLOUR('',#18318);
#18320=FILL_AREA_STYLE('',(#18319));
#18321=SURFACE_STYLE_FILL_AREA(#18320);
#18322=SURFACE_SIDE_STYLE('',(#18321));
#18323=SURFACE_STYLE_USAGE(.BOTH.,#18322);
#18324=PRESENTATION_STYLE_ASSIGNMENT((#18323));
ENDSEC;
END-ISO-10303-21;
